ISO-10303-21;
HEADER;
FILE_DESCRIPTION (('STEP AP214'),
    '1' );
FILE_NAME ('Cap Ring.step',
    '2026-10-06T14:00:01',
    ( '' ),
    ( '' ),
    'SwSTEP 2.0',
    'SolidWorks 2020',
    '' );
FILE_SCHEMA (( 'AUTOMOTIVE_DESIGN' ));
ENDSEC;

DATA;
#154=ORIENTED_EDGE ( 'NONE', *, *, #27235, .T. ) ;
#327=AXIS2_PLACEMENT_3D ( 'NONE', #3583, #20536, #15450 ) ;
#468=VERTEX_POINT ( 'NONE', #17898 ) ;
#1070=CARTESIAN_POINT ( 'NONE',  ( -57.22499999999997300, 2.964020293532818446E-15, 1.549317489258324336E-18 ) ) ;
#1294=( LENGTH_UNIT ( ) NAMED_UNIT ( * ) SI_UNIT ( .MILLI., .METRE. ) );
#1417=PRODUCT_CONTEXT ( 'NONE', #25911, 'mechanical' ) ;
#1471=DIRECTION ( 'NONE',  ( 0.000000000000000000, 1.000000000000000000, 0.000000000000000000 ) ) ;
#1561=SHAPE_REPRESENTATION ( 'Cap Ring', ( #9018 ), #12557 ) ;
#1742=CIRCLE ( 'NONE', #25547, 0.4999999999999996114 ) ;
#1757=( NAMED_UNIT ( * ) PLANE_ANGLE_UNIT ( ) SI_UNIT ( $, .RADIAN. ) );
#1945=( GEOMETRIC_REPRESENTATION_CONTEXT ( 3 ) GLOBAL_UNCERTAINTY_ASSIGNED_CONTEXT ( ( #6994 ) ) GLOBAL_UNIT_ASSIGNED_CONTEXT ( ( #26465, #6678, #26158 ) ) REPRESENTATION_CONTEXT ( 'NONE', 'WORKASPACE' ) );
#1977=ORIENTED_EDGE ( 'NONE', *, *, #30437, .T. ) ;
#2084=SHAPE_REPRESENTATION_RELATIONSHIP ( 'NONE' , 'NONE' ,  #1561, #15356 ) ;
#2114=EDGE_LOOP ( 'NONE', ( #16744, #13809, #12837, #23029 ) ) ;
#2524=DIRECTION ( 'NONE',  ( 0.000000000000000000, 1.000000000000000000, 0.000000000000000000 ) ) ;
#2847=ADVANCED_FACE ( 'NONE', ( #27640 ), #4004, .T. ) ;
#3152=ORIENTED_EDGE ( 'NONE', *, *, #27235, .F. ) ;
#3294=DIRECTION ( 'NONE',  ( 1.000000000000000000, 3.054025858079668409E-16, -2.042474015755241579E-16 ) ) ;
#3364=TOROIDAL_SURFACE ( 'NONE', #18041, 4.600000000000000533, 0.4999999999999996669 ) ;
#3480=UNCERTAINTY_MEASURE_WITH_UNIT (LENGTH_MEASURE( 1.000000000000000082E-05 ), #21645, 'distance_accuracy_value', 'NONE');
#3583=CARTESIAN_POINT ( 'NONE',  ( -57.22499999999997300, 0.9241234443029104906, -4.506217466977124886 ) ) ;
#3832=TOROIDAL_SURFACE ( 'NONE', #29130, 4.600000000000000533, 0.4999999999999996669 ) ;
#3841=MECHANICAL_DESIGN_GEOMETRIC_PRESENTATION_REPRESENTATION('',(#23098),#17027);
#4004=TOROIDAL_SURFACE ( 'NONE', #29791, 4.600000000000000533, 0.4999999999999996669 ) ;
#4519=SURFACE_STYLE_USAGE ( .BOTH. , #20996 ) ;
#4615=FILL_AREA_STYLE_COLOUR ( '', #17130 ) ;
#4720=CARTESIAN_POINT ( 'NONE',  ( -57.22499999999997300, -0.9241234443029052725, 4.506217466977124886 ) ) ;
#5302=AXIS2_PLACEMENT_3D ( 'NONE', #21387, #23752, #19001 ) ;
#5688=PRODUCT_DEFINITION_CONTEXT ( 'detailed design', #27395, 'design' ) ;
#5769=ORIENTED_EDGE ( 'NONE', *, *, #17993, .T. ) ;
#5873=DIRECTION ( 'NONE',  ( 1.000000000000000000, 3.054025858079668409E-16, -2.042474015755241579E-16 ) ) ;
#5958=EDGE_CURVE ( 'NONE', #25169, #468, #23140, .T. ) ;
#6081=CARTESIAN_POINT ( 'NONE',  ( -57.22499999999997300, 0.9241234443029104906, -4.506217466977124886 ) ) ;
#6082=CARTESIAN_POINT ( 'NONE',  ( -57.22499999999997300, 2.964020293532818446E-15, 1.549317489258312010E-18 ) ) ;
#6382=DIRECTION ( 'NONE',  ( 1.000000000000000000, 3.054025858079668409E-16, -2.042474015755241579E-16 ) ) ;
#6432=DIRECTION ( 'NONE',  ( -2.581436205204234499E-16, 0.9796124928211140670, 0.2008964009354147762 ) ) ;
#6460=CARTESIAN_POINT ( 'NONE',  ( -57.22499999999997300, 0.8236752438352032968, -4.016411220566568296 ) ) ;
#6678=( NAMED_UNIT ( * ) PLANE_ANGLE_UNIT ( ) SI_UNIT ( $, .RADIAN. ) );
#6834=FILL_AREA_STYLE ('',( #4615 ) ) ;
#6994=UNCERTAINTY_MEASURE_WITH_UNIT (LENGTH_MEASURE( 1.000000000000000082E-05 ), #26465, 'distance_accuracy_value', 'NONE');
#7164=SURFACE_STYLE_FILL_AREA ( #6834 ) ;
#7257=DIRECTION ( 'NONE',  ( 1.000000000000000000, 3.054025858079668409E-16, -2.042474015755241579E-16 ) ) ;
#7369=ORIENTED_EDGE ( 'NONE', *, *, #23352, .F. ) ;
#7427=DIRECTION ( 'NONE',  ( 0.000000000000000000, -0.2008964009354146929, 0.9796124928211140670 ) ) ;
#7520=DIRECTION ( 'NONE',  ( 2.614375865348241018E-16, -0.2008964009354148039, 0.9796124928211140670 ) ) ;
#7900=ORIENTED_EDGE ( 'NONE', *, *, #30437, .F. ) ;
#7986=CIRCLE ( 'NONE', #25674, 5.100000000000000533 ) ;
#8241=DIRECTION ( 'NONE',  ( 2.614375865348241018E-16, -0.2008964009354148039, 0.9796124928211140670 ) ) ;
#9018=AXIS2_PLACEMENT_3D ( 'NONE', #25987, #9060, #11596 ) ;
#9060=DIRECTION ( 'NONE',  ( 0.000000000000000000, 0.000000000000000000, 1.000000000000000000 ) ) ;
#9147=VERTEX_POINT ( 'NONE', #28099 ) ;
#9553=SURFACE_STYLE_USAGE ( .BOTH. , #18733 ) ;
#10237=CIRCLE ( 'NONE', #30458, 0.4999999999999996114 ) ;
#10272=PRODUCT_DEFINITION ( 'UNKNOWN', '', #13626, #5688 ) ;
#10470=CLOSED_SHELL ( 'NONE', ( #16351, #13427, #17251, #2847 ) ) ;
#11388=AXIS2_PLACEMENT_3D ( 'NONE', #12400, #14928, #7520 ) ;
#11441=COLOUR_RGB ( '', 0.40784314, 0.44705882, 0.49803922) ;
#11596=DIRECTION ( 'NONE',  ( 1.000000000000000000, 0.000000000000000000, 0.000000000000000000 ) ) ;
#12112=FACE_OUTER_BOUND ( 'NONE', #2114, .T. ) ;
#12400=CARTESIAN_POINT ( 'NONE',  ( -57.22499999999997300, 2.964020293532818446E-15, 1.549317489258312010E-18 ) ) ;
#12557=( GEOMETRIC_REPRESENTATION_CONTEXT ( 3 ) GLOBAL_UNCERTAINTY_ASSIGNED_CONTEXT ( ( #28834 ) ) GLOBAL_UNIT_ASSIGNED_CONTEXT ( ( #1294, #1757, #14117 ) ) REPRESENTATION_CONTEXT ( 'NONE', 'WORKASPACE' ) );
#12837=ORIENTED_EDGE ( 'NONE', *, *, #23352, .T. ) ;
#13218=DIRECTION ( 'NONE',  ( 2.614375865348241018E-16, -0.2008964009354148039, 0.9796124928211140670 ) ) ;
#13251=CIRCLE ( 'NONE', #25901, 0.4999999999999996114 ) ;
#13427=ADVANCED_FACE ( 'NONE', ( #29975 ), #3364, .T. ) ;
#13626=PRODUCT_DEFINITION_FORMATION_WITH_SPECIFIED_SOURCE ( 'ANY', '', #23518, .NOT_KNOWN. ) ;
#13809=ORIENTED_EDGE ( 'NONE', *, *, #22998, .T. ) ;
#14004=( NAMED_UNIT ( * ) PLANE_ANGLE_UNIT ( ) SI_UNIT ( $, .RADIAN. ) );
#14117=( NAMED_UNIT ( * ) SI_UNIT ( $, .STERADIAN. ) SOLID_ANGLE_UNIT ( ) );
#14170=FILL_AREA_STYLE ('',( #31108 ) ) ;
#14928=DIRECTION ( 'NONE',  ( 1.000000000000000000, 3.054025858079668409E-16, -2.042474015755241579E-16 ) ) ;
#14932=TOROIDAL_SURFACE ( 'NONE', #11388, 4.600000000000000533, 0.4999999999999996669 ) ;
#15356=ADVANCED_BREP_SHAPE_REPRESENTATION ( '', ( #25800, #9018 ), #12557 ) ;
#15412=DIRECTION ( 'NONE',  ( 0.000000000000000000, 0.2008964009354144709, -0.9796124928211140670 ) ) ;
#15450=DIRECTION ( 'NONE',  ( 0.000000000000000000, 0.2008964009354144709, -0.9796124928211140670 ) ) ;
#15643=DIRECTION ( 'NONE',  ( 0.000000000000000000, 1.000000000000000000, 0.000000000000000000 ) ) ;
#16351=ADVANCED_FACE ( 'NONE', ( #12112 ), #14932, .T. ) ;
#16393=( NAMED_UNIT ( * ) SI_UNIT ( $, .STERADIAN. ) SOLID_ANGLE_UNIT ( ) );
#16633=MECHANICAL_DESIGN_GEOMETRIC_PRESENTATION_REPRESENTATION('',(#21708),#1945);
#16744=ORIENTED_EDGE ( 'NONE', *, *, #17993, .F. ) ;
#17027=( GEOMETRIC_REPRESENTATION_CONTEXT ( 3 ) GLOBAL_UNCERTAINTY_ASSIGNED_CONTEXT ( ( #3480 ) ) GLOBAL_UNIT_ASSIGNED_CONTEXT ( ( #21645, #14004, #16393 ) ) REPRESENTATION_CONTEXT ( 'NONE', 'WORKASPACE' ) );
#17130=COLOUR_RGB ( '', 0.40784314, 0.44705882, 0.49803922) ;
#17145=CARTESIAN_POINT ( 'NONE',  ( -57.22499999999997300, 2.964020293532818446E-15, 1.549317489258312010E-18 ) ) ;
#17251=ADVANCED_FACE ( 'NONE', ( #21754 ), #3832, .T. ) ;
#17348=EDGE_LOOP ( 'NONE', ( #23942, #19882, #25546, #29842 ) ) ;
#17577=AXIS2_PLACEMENT_3D ( 'NONE', #1070, #24816, #15643 ) ;
#17808=DIRECTION ( 'NONE',  ( 2.581436205204234499E-16, -0.9796124928211140670, -0.2008964009354146651 ) ) ;
#17898=CARTESIAN_POINT ( 'NONE',  ( -57.22499999999997300, -0.8236752438351979677, 4.016411220566568296 ) ) ;
#17993=EDGE_CURVE ( 'NONE', #19884, #25169, #1742, .T. ) ;
#18041=AXIS2_PLACEMENT_3D ( 'NONE', #6082, #3294, #20653 ) ;
#18530=SHAPE_DEFINITION_REPRESENTATION ( #30574, #1561 ) ;
#18629=SURFACE_STYLE_FILL_AREA ( #14170 ) ;
#18733=SURFACE_SIDE_STYLE ('',( #7164 ) ) ;
#18789=DIRECTION ( 'NONE',  ( 0.000000000000000000, -0.2008964009354146929, 0.9796124928211140670 ) ) ;
#19001=DIRECTION ( 'NONE',  ( 0.000000000000000000, 1.000000000000000000, 0.000000000000000000 ) ) ;
#19452=EDGE_LOOP ( 'NONE', ( #7369, #1977, #5769, #3152 ) ) ;
#19882=ORIENTED_EDGE ( 'NONE', *, *, #25639, .F. ) ;
#19884=VERTEX_POINT ( 'NONE', #31142 ) ;
#20536=DIRECTION ( 'NONE',  ( 2.581436205204234499E-16, -0.9796124928211140670, -0.2008964009354146651 ) ) ;
#20653=DIRECTION ( 'NONE',  ( 2.614375865348241018E-16, -0.2008964009354148039, 0.9796124928211140670 ) ) ;
#20996=SURFACE_SIDE_STYLE ('',( #18629 ) ) ;
#21387=CARTESIAN_POINT ( 'NONE',  ( -57.22499999999997300, 2.964020293532818446E-15, 1.549317489258312010E-18 ) ) ;
#21645=( LENGTH_UNIT ( ) NAMED_UNIT ( * ) SI_UNIT ( .MILLI., .METRE. ) );
#21708=STYLED_ITEM ( 'NONE', ( #31052 ), #15356 ) ;
#21754=FACE_OUTER_BOUND ( 'NONE', #27437, .T. ) ;
#22755=DIRECTION ( 'NONE',  ( 1.000000000000000000, 3.054025858079668409E-16, -2.042474015755241579E-16 ) ) ;
#22998=EDGE_CURVE ( 'NONE', #19884, #9147, #24515, .T. ) ;
#23029=ORIENTED_EDGE ( 'NONE', *, *, #5958, .F. ) ;
#23091=CIRCLE ( 'NONE', #24585, 4.100000000000001421 ) ;
#23098=STYLED_ITEM ( 'NONE', ( #23844 ), #25800 ) ;
#23140=CIRCLE ( 'NONE', #17577, 4.100000000000001421 ) ;
#23212=EDGE_CURVE ( 'NONE', #468, #9147, #13251, .T. ) ;
#23261=CARTESIAN_POINT ( 'NONE',  ( -57.22499999999997300, 2.964020293532818446E-15, 1.549317489258312010E-18 ) ) ;
#23352=EDGE_CURVE ( 'NONE', #9147, #468, #10237, .T. ) ;
#23518=PRODUCT ( 'Cap Ring', 'Cap Ring', '', ( #1417 ) ) ;
#23752=DIRECTION ( 'NONE',  ( 1.000000000000000000, 3.054025858079668409E-16, -2.042474015755241579E-16 ) ) ;
#23844=PRESENTATION_STYLE_ASSIGNMENT (( #4519 ) ) ;
#23942=ORIENTED_EDGE ( 'NONE', *, *, #22998, .F. ) ;
#24515=CIRCLE ( 'NONE', #5302, 5.100000000000000533 ) ;
#24585=AXIS2_PLACEMENT_3D ( 'NONE', #25386, #6382, #1471 ) ;
#24816=DIRECTION ( 'NONE',  ( 1.000000000000000000, 3.054025858079668409E-16, -2.042474015755241579E-16 ) ) ;
#25169=VERTEX_POINT ( 'NONE', #6460 ) ;
#25386=CARTESIAN_POINT ( 'NONE',  ( -57.22499999999997300, 2.964020293532818446E-15, 1.549317489258324336E-18 ) ) ;
#25416=CARTESIAN_POINT ( 'NONE',  ( -57.22499999999997300, 2.964020293532818446E-15, 1.549317489258312010E-18 ) ) ;
#25546=ORIENTED_EDGE ( 'NONE', *, *, #5958, .T. ) ;
#25547=AXIS2_PLACEMENT_3D ( 'NONE', #6081, #17808, #15412 ) ;
#25639=EDGE_CURVE ( 'NONE', #25169, #19884, #27627, .T. ) ;
#25674=AXIS2_PLACEMENT_3D ( 'NONE', #23261, #7257, #2524 ) ;
#25800=MANIFOLD_SOLID_BREP ( 'Stock-MAS-683-1', #10470 ) ;
#25901=AXIS2_PLACEMENT_3D ( 'NONE', #4720, #28953, #7427 ) ;
#25911=APPLICATION_CONTEXT ( 'automotive_design' ) ;
#25987=CARTESIAN_POINT ( 'NONE',  ( 0.000000000000000000, 0.000000000000000000, 0.000000000000000000 ) ) ;
#26061=ORIENTED_EDGE ( 'NONE', *, *, #23212, .F. ) ;
#26158=( NAMED_UNIT ( * ) SI_UNIT ( $, .STERADIAN. ) SOLID_ANGLE_UNIT ( ) );
#26465=( LENGTH_UNIT ( ) NAMED_UNIT ( * ) SI_UNIT ( .MILLI., .METRE. ) );
#27235=EDGE_CURVE ( 'NONE', #468, #25169, #23091, .T. ) ;
#27395=APPLICATION_CONTEXT ( 'automotive_design' ) ;
#27437=EDGE_LOOP ( 'NONE', ( #7900, #26061, #154, #27887 ) ) ;
#27627=CIRCLE ( 'NONE', #327, 0.4999999999999996114 ) ;
#27640=FACE_OUTER_BOUND ( 'NONE', #17348, .T. ) ;
#27887=ORIENTED_EDGE ( 'NONE', *, *, #25639, .T. ) ;
#28099=CARTESIAN_POINT ( 'NONE',  ( -57.22499999999997300, -1.024571644770612577, 4.996023713387681475 ) ) ;
#28834=UNCERTAINTY_MEASURE_WITH_UNIT (LENGTH_MEASURE( 1.000000000000000082E-05 ), #1294, 'distance_accuracy_value', 'NONE');
#28953=DIRECTION ( 'NONE',  ( -2.581436205204234499E-16, 0.9796124928211140670, 0.2008964009354147762 ) ) ;
#29130=AXIS2_PLACEMENT_3D ( 'NONE', #17145, #5873, #8241 ) ;
#29791=AXIS2_PLACEMENT_3D ( 'NONE', #25416, #22755, #13218 ) ;
#29842=ORIENTED_EDGE ( 'NONE', *, *, #23212, .T. ) ;
#29975=FACE_OUTER_BOUND ( 'NONE', #19452, .T. ) ;
#30437=EDGE_CURVE ( 'NONE', #9147, #19884, #7986, .T. ) ;
#30458=AXIS2_PLACEMENT_3D ( 'NONE', #30964, #6432, #18789 ) ;
#30574=PRODUCT_DEFINITION_SHAPE ( 'NONE', 'NONE',  #10272 ) ;
#30964=CARTESIAN_POINT ( 'NONE',  ( -57.22499999999997300, -0.9241234443029052725, 4.506217466977124886 ) ) ;
#31052=PRESENTATION_STYLE_ASSIGNMENT (( #9553 ) ) ;
#31108=FILL_AREA_STYLE_COLOUR ( '', #11441 ) ;
#31142=CARTESIAN_POINT ( 'NONE',  ( -57.22499999999997300, 1.024571644770617684, -4.996023713387681475 ) ) ;
ENDSEC;
END-ISO-10303-21;
